ISO-10303-21;
HEADER;
/* Generated by software containing ST-Developer
 * from STEP Tools, Inc. (www.steptools.com) 
 */

FILE_DESCRIPTION(
/* description */ ('PAT-082'),
/* implementation_level */ '2;1');

FILE_NAME(
/* name */ 'M4x10 Cap Screw.step',
/* time_stamp */ '2026-10-29T20:16:13-07:00',
/* author */ (''),
/* organization */ (''),
/* preprocessor_version */ 'ST-DEVELOPER v20.2',
/* originating_system */ 'Autodesk Translation Framework v15.17.0.0',
/* authorisation */ '');

FILE_SCHEMA (('AUTOMOTIVE_DESIGN { 1 0 10303 214 3 1 1 }'));
ENDSEC;

DATA;
#10=MECHANICAL_DESIGN_GEOMETRIC_PRESENTATION_REPRESENTATION('',(#262),#8266);
#176=CONICAL_SURFACE('',#5334,0.325,0.785398163397448);
#177=CONICAL_SURFACE('',#5338,0.335,0.785398163397448);
#178=CONICAL_SURFACE('',#5342,0.21,0.463647609000806);
#181=ORIENTED_CLOSED_SHELL('',*,#4604,.F.);
#184=BREP_WITH_VOIDS('Body1',#4605,(#181));
#218=SHAPE_REPRESENTATION_RELATIONSHIP('SRR','None',#8381,#240);
#240=ADVANCED_BREP_SHAPE_REPRESENTATION('',(#184),#8265);
#262=STYLED_ITEM('',(#8544),#184);
#404=FACE_BOUND('',#1232,.T.);
#561=PLANE('',#5322);
#562=PLANE('',#5323);
#563=PLANE('',#5324);
#564=PLANE('',#5325);
#565=PLANE('',#5326);
#566=PLANE('',#5327);
#567=PLANE('',#5328);
#568=PLANE('',#5329);
#569=PLANE('',#5330);
#570=PLANE('',#5332);
#571=PLANE('',#5340);
#826=FACE_OUTER_BOUND('',#1218,.T.);
#827=FACE_OUTER_BOUND('',#1219,.T.);
#828=FACE_OUTER_BOUND('',#1220,.T.);
#829=FACE_OUTER_BOUND('',#1221,.T.);
#830=FACE_OUTER_BOUND('',#1222,.T.);
#831=FACE_OUTER_BOUND('',#1223,.T.);
#832=FACE_OUTER_BOUND('',#1224,.T.);
#833=FACE_OUTER_BOUND('',#1225,.T.);
#834=FACE_OUTER_BOUND('',#1226,.T.);
#835=FACE_OUTER_BOUND('',#1227,.T.);
#836=FACE_OUTER_BOUND('',#1228,.T.);
#837=FACE_OUTER_BOUND('',#1229,.T.);
#838=FACE_OUTER_BOUND('',#1230,.T.);
#839=FACE_OUTER_BOUND('',#1231,.T.);
#840=FACE_OUTER_BOUND('',#1233,.T.);
#841=FACE_OUTER_BOUND('',#1234,.T.);
#1218=EDGE_LOOP('',(#4160,#4161,#4162,#4163));
#1219=EDGE_LOOP('',(#4164,#4165,#4166,#4167));
#1220=EDGE_LOOP('',(#4168,#4169,#4170,#4171));
#1221=EDGE_LOOP('',(#4172,#4173,#4174,#4175));
#1222=EDGE_LOOP('',(#4176,#4177,#4178,#4179));
#1223=EDGE_LOOP('',(#4180,#4181,#4182,#4183));
#1224=EDGE_LOOP('',(#4184,#4185,#4186,#4187,#4188,#4189));
#1225=EDGE_LOOP('',(#4190,#4191,#4192,#4193,#4194,#4195));
#1226=EDGE_LOOP('',(#4196));
#1227=EDGE_LOOP('',(#4197));
#1228=EDGE_LOOP('',(#4198,#4199,#4200,#4201));
#1229=EDGE_LOOP('',(#4202,#4203,#4204,#4205));
#1230=EDGE_LOOP('',(#4206,#4207,#4208,#4209));
#1231=EDGE_LOOP('',(#4210));
#1232=EDGE_LOOP('',(#4211));
#1233=EDGE_LOOP('',(#4212,#4213,#4214,#4215));
#1234=EDGE_LOOP('',(#4216,#4217,#4218,#4219));
#1567=LINE('',#8118,#1922);
#1568=LINE('',#8120,#1923);
#1569=LINE('',#8122,#1924);
#1570=LINE('',#8123,#1925);
#1571=LINE('',#8126,#1926);
#1572=LINE('',#8128,#1927);
#1573=LINE('',#8129,#1928);
#1574=LINE('',#8132,#1929);
#1575=LINE('',#8134,#1930);
#1576=LINE('',#8135,#1931);
#1577=LINE('',#8138,#1932);
#1578=LINE('',#8140,#1933);
#1579=LINE('',#8141,#1934);
#1580=LINE('',#8144,#1935);
#1581=LINE('',#8146,#1936);
#1582=LINE('',#8147,#1937);
#1583=LINE('',#8149,#1938);
#1584=LINE('',#8150,#1939);
#1585=LINE('',#8162,#1940);
#1586=LINE('',#8166,#1941);
#1587=LINE('',#8170,#1942);
#1588=LINE('',#8177,#1943);
#1589=LINE('',#8179,#1944);
#1922=VECTOR('',#6662,1.);
#1923=VECTOR('',#6663,1.);
#1924=VECTOR('',#6664,1.);
#1925=VECTOR('',#6665,1.);
#1926=VECTOR('',#6668,1.);
#1927=VECTOR('',#6669,1.);
#1928=VECTOR('',#6670,1.);
#1929=VECTOR('',#6673,1.);
#1930=VECTOR('',#6674,1.);
#1931=VECTOR('',#6675,1.);
#1932=VECTOR('',#6678,1.);
#1933=VECTOR('',#6679,1.);
#1934=VECTOR('',#6680,1.);
#1935=VECTOR('',#6683,1.);
#1936=VECTOR('',#6684,1.);
#1937=VECTOR('',#6685,1.);
#1938=VECTOR('',#6688,1.);
#1939=VECTOR('',#6689,1.);
#1940=VECTOR('',#6706,0.325);
#1941=VECTOR('',#6711,0.35);
#1942=VECTOR('',#6716,0.335);
#1943=VECTOR('',#6725,0.21);
#1944=VECTOR('',#6728,0.2);
#2138=CIRCLE('',#5331,0.1954);
#2139=CIRCLE('',#5333,0.3);
#2140=CIRCLE('',#5335,0.35);
#2141=CIRCLE('',#5337,0.35);
#2142=CIRCLE('',#5339,0.32);
#2143=CIRCLE('',#5341,0.22);
#2144=CIRCLE('',#5343,0.1954);
#2500=VERTEX_POINT('',#8116);
#2501=VERTEX_POINT('',#8117);
#2502=VERTEX_POINT('',#8119);
#2503=VERTEX_POINT('',#8121);
#2504=VERTEX_POINT('',#8125);
#2505=VERTEX_POINT('',#8127);
#2506=VERTEX_POINT('',#8131);
#2507=VERTEX_POINT('',#8133);
#2508=VERTEX_POINT('',#8137);
#2509=VERTEX_POINT('',#8139);
#2510=VERTEX_POINT('',#8143);
#2511=VERTEX_POINT('',#8145);
#2512=VERTEX_POINT('',#8154);
#2513=VERTEX_POINT('',#8157);
#2514=VERTEX_POINT('',#8160);
#2515=VERTEX_POINT('',#8164);
#2516=VERTEX_POINT('',#8168);
#2517=VERTEX_POINT('',#8172);
#2518=VERTEX_POINT('',#8175);
#3056=EDGE_CURVE('',#2500,#2501,#1567,.T.);
#3057=EDGE_CURVE('',#2501,#2502,#1568,.T.);
#3058=EDGE_CURVE('',#2502,#2503,#1569,.T.);
#3059=EDGE_CURVE('',#2500,#2503,#1570,.T.);
#3060=EDGE_CURVE('',#2501,#2504,#1571,.T.);
#3061=EDGE_CURVE('',#2504,#2505,#1572,.T.);
#3062=EDGE_CURVE('',#2505,#2502,#1573,.T.);
#3063=EDGE_CURVE('',#2504,#2506,#1574,.T.);
#3064=EDGE_CURVE('',#2506,#2507,#1575,.T.);
#3065=EDGE_CURVE('',#2507,#2505,#1576,.T.);
#3066=EDGE_CURVE('',#2506,#2508,#1577,.T.);
#3067=EDGE_CURVE('',#2508,#2509,#1578,.T.);
#3068=EDGE_CURVE('',#2509,#2507,#1579,.T.);
#3069=EDGE_CURVE('',#2508,#2510,#1580,.T.);
#3070=EDGE_CURVE('',#2510,#2511,#1581,.T.);
#3071=EDGE_CURVE('',#2511,#2509,#1582,.T.);
#3072=EDGE_CURVE('',#2510,#2500,#1583,.T.);
#3073=EDGE_CURVE('',#2503,#2511,#1584,.T.);
#3074=EDGE_CURVE('',#2512,#2512,#2138,.T.);
#3075=EDGE_CURVE('',#2513,#2513,#2139,.T.);
#3076=EDGE_CURVE('',#2514,#2514,#2140,.T.);
#3077=EDGE_CURVE('',#2514,#2513,#1585,.T.);
#3078=EDGE_CURVE('',#2515,#2515,#2141,.T.);
#3079=EDGE_CURVE('',#2515,#2514,#1586,.T.);
#3080=EDGE_CURVE('',#2516,#2516,#2142,.T.);
#3081=EDGE_CURVE('',#2516,#2515,#1587,.T.);
#3082=EDGE_CURVE('',#2517,#2517,#2143,.T.);
#3083=EDGE_CURVE('',#2518,#2518,#2144,.F.);
#3084=EDGE_CURVE('',#2518,#2517,#1588,.T.);
#3085=EDGE_CURVE('',#2512,#2518,#1589,.T.);
#4160=ORIENTED_EDGE('',*,*,#3056,.T.);
#4161=ORIENTED_EDGE('',*,*,#3057,.T.);
#4162=ORIENTED_EDGE('',*,*,#3058,.T.);
#4163=ORIENTED_EDGE('',*,*,#3059,.F.);
#4164=ORIENTED_EDGE('',*,*,#3060,.T.);
#4165=ORIENTED_EDGE('',*,*,#3061,.T.);
#4166=ORIENTED_EDGE('',*,*,#3062,.T.);
#4167=ORIENTED_EDGE('',*,*,#3057,.F.);
#4168=ORIENTED_EDGE('',*,*,#3063,.T.);
#4169=ORIENTED_EDGE('',*,*,#3064,.T.);
#4170=ORIENTED_EDGE('',*,*,#3065,.T.);
#4171=ORIENTED_EDGE('',*,*,#3061,.F.);
#4172=ORIENTED_EDGE('',*,*,#3066,.T.);
#4173=ORIENTED_EDGE('',*,*,#3067,.T.);
#4174=ORIENTED_EDGE('',*,*,#3068,.T.);
#4175=ORIENTED_EDGE('',*,*,#3064,.F.);
#4176=ORIENTED_EDGE('',*,*,#3069,.T.);
#4177=ORIENTED_EDGE('',*,*,#3070,.T.);
#4178=ORIENTED_EDGE('',*,*,#3071,.T.);
#4179=ORIENTED_EDGE('',*,*,#3067,.F.);
#4180=ORIENTED_EDGE('',*,*,#3072,.T.);
#4181=ORIENTED_EDGE('',*,*,#3059,.T.);
#4182=ORIENTED_EDGE('',*,*,#3073,.T.);
#4183=ORIENTED_EDGE('',*,*,#3070,.F.);
#4184=ORIENTED_EDGE('',*,*,#3072,.F.);
#4185=ORIENTED_EDGE('',*,*,#3069,.F.);
#4186=ORIENTED_EDGE('',*,*,#3066,.F.);
#4187=ORIENTED_EDGE('',*,*,#3063,.F.);
#4188=ORIENTED_EDGE('',*,*,#3060,.F.);
#4189=ORIENTED_EDGE('',*,*,#3056,.F.);
#4190=ORIENTED_EDGE('',*,*,#3073,.F.);
#4191=ORIENTED_EDGE('',*,*,#3058,.F.);
#4192=ORIENTED_EDGE('',*,*,#3062,.F.);
#4193=ORIENTED_EDGE('',*,*,#3065,.F.);
#4194=ORIENTED_EDGE('',*,*,#3068,.F.);
#4195=ORIENTED_EDGE('',*,*,#3071,.F.);
#4196=ORIENTED_EDGE('',*,*,#3074,.F.);
#4197=ORIENTED_EDGE('',*,*,#3075,.F.);
#4198=ORIENTED_EDGE('',*,*,#3076,.F.);
#4199=ORIENTED_EDGE('',*,*,#3077,.T.);
#4200=ORIENTED_EDGE('',*,*,#3075,.T.);
#4201=ORIENTED_EDGE('',*,*,#3077,.F.);
#4202=ORIENTED_EDGE('',*,*,#3078,.F.);
#4203=ORIENTED_EDGE('',*,*,#3079,.T.);
#4204=ORIENTED_EDGE('',*,*,#3076,.T.);
#4205=ORIENTED_EDGE('',*,*,#3079,.F.);
#4206=ORIENTED_EDGE('',*,*,#3080,.F.);
#4207=ORIENTED_EDGE('',*,*,#3081,.T.);
#4208=ORIENTED_EDGE('',*,*,#3078,.T.);
#4209=ORIENTED_EDGE('',*,*,#3081,.F.);
#4210=ORIENTED_EDGE('',*,*,#3080,.T.);
#4211=ORIENTED_EDGE('',*,*,#3082,.F.);
#4212=ORIENTED_EDGE('',*,*,#3083,.F.);
#4213=ORIENTED_EDGE('',*,*,#3084,.T.);
#4214=ORIENTED_EDGE('',*,*,#3082,.T.);
#4215=ORIENTED_EDGE('',*,*,#3084,.F.);
#4216=ORIENTED_EDGE('',*,*,#3074,.T.);
#4217=ORIENTED_EDGE('',*,*,#3085,.T.);
#4218=ORIENTED_EDGE('',*,*,#3083,.T.);
#4219=ORIENTED_EDGE('',*,*,#3085,.F.);
#4309=CYLINDRICAL_SURFACE('',#5336,0.35);
#4310=CYLINDRICAL_SURFACE('',#5344,0.1954);
#4565=ADVANCED_FACE('',(#826),#561,.F.);
#4566=ADVANCED_FACE('',(#827),#562,.F.);
#4567=ADVANCED_FACE('',(#828),#563,.F.);
#4568=ADVANCED_FACE('',(#829),#564,.F.);
#4569=ADVANCED_FACE('',(#830),#565,.F.);
#4570=ADVANCED_FACE('',(#831),#566,.F.);
#4571=ADVANCED_FACE('',(#832),#567,.F.);
#4572=ADVANCED_FACE('',(#833),#568,.F.);
#4573=ADVANCED_FACE('',(#834),#569,.F.);
#4574=ADVANCED_FACE('',(#835),#570,.T.);
#4575=ADVANCED_FACE('',(#836),#176,.T.);
#4576=ADVANCED_FACE('',(#837),#4309,.T.);
#4577=ADVANCED_FACE('',(#838),#177,.T.);
#4578=ADVANCED_FACE('',(#839,#404),#571,.T.);
#4579=ADVANCED_FACE('',(#840),#178,.T.);
#4580=ADVANCED_FACE('',(#841),#4310,.T.);
#4604=CLOSED_SHELL('',(#4565,#4566,#4567,#4568,#4569,#4570,#4571,#4572));
#4605=CLOSED_SHELL('',(#4573,#4574,#4575,#4576,#4577,#4578,#4579,#4580));
#5321=AXIS2_PLACEMENT_3D('',#8114,#6658,#6659);
#5322=AXIS2_PLACEMENT_3D('',#8115,#6660,#6661);
#5323=AXIS2_PLACEMENT_3D('',#8124,#6666,#6667);
#5324=AXIS2_PLACEMENT_3D('',#8130,#6671,#6672);
#5325=AXIS2_PLACEMENT_3D('',#8136,#6676,#6677);
#5326=AXIS2_PLACEMENT_3D('',#8142,#6681,#6682);
#5327=AXIS2_PLACEMENT_3D('',#8148,#6686,#6687);
#5328=AXIS2_PLACEMENT_3D('',#8151,#6690,#6691);
#5329=AXIS2_PLACEMENT_3D('',#8152,#6692,#6693);
#5330=AXIS2_PLACEMENT_3D('',#8153,#6694,#6695);
#5331=AXIS2_PLACEMENT_3D('',#8155,#6696,#6697);
#5332=AXIS2_PLACEMENT_3D('',#8156,#6698,#6699);
#5333=AXIS2_PLACEMENT_3D('',#8158,#6700,#6701);
#5334=AXIS2_PLACEMENT_3D('',#8159,#6702,#6703);
#5335=AXIS2_PLACEMENT_3D('',#8161,#6704,#6705);
#5336=AXIS2_PLACEMENT_3D('',#8163,#6707,#6708);
#5337=AXIS2_PLACEMENT_3D('',#8165,#6709,#6710);
#5338=AXIS2_PLACEMENT_3D('',#8167,#6712,#6713);
#5339=AXIS2_PLACEMENT_3D('',#8169,#6714,#6715);
#5340=AXIS2_PLACEMENT_3D('',#8171,#6717,#6718);
#5341=AXIS2_PLACEMENT_3D('',#8173,#6719,#6720);
#5342=AXIS2_PLACEMENT_3D('',#8174,#6721,#6722);
#5343=AXIS2_PLACEMENT_3D('',#8176,#6723,#6724);
#5344=AXIS2_PLACEMENT_3D('',#8178,#6726,#6727);
#6658=DIRECTION('axis',(0.,0.,1.));
#6659=DIRECTION('refdir',(1.,0.,0.));
#6660=DIRECTION('center_axis',(0.866025403784439,0.,-0.5));
#6661=DIRECTION('ref_axis',(0.5,0.,0.866025403784439));
#6662=DIRECTION('',(-0.5,0.,-0.866025403784439));
#6663=DIRECTION('',(0.,-1.,0.));
#6664=DIRECTION('',(0.5,0.,0.866025403784439));
#6665=DIRECTION('',(0.,-1.,0.));
#6666=DIRECTION('center_axis',(1.60246890531964E-16,0.,-1.));
#6667=DIRECTION('ref_axis',(1.,0.,1.60246890531964E-16));
#6668=DIRECTION('',(-1.,0.,-1.60246890531964E-16));
#6669=DIRECTION('',(0.,-1.,0.));
#6670=DIRECTION('',(1.,0.,1.60246890531964E-16));
#6671=DIRECTION('center_axis',(-0.866025403784439,0.,-0.5));
#6672=DIRECTION('ref_axis',(0.5,0.,-0.866025403784439));
#6673=DIRECTION('',(-0.5,0.,0.866025403784439));
#6674=DIRECTION('',(0.,-1.,0.));
#6675=DIRECTION('',(0.5,0.,-0.866025403784439));
#6676=DIRECTION('center_axis',(-0.866025403784439,0.,0.5));
#6677=DIRECTION('ref_axis',(-0.5,0.,-0.866025403784439));
#6678=DIRECTION('',(0.5,0.,0.866025403784439));
#6679=DIRECTION('',(0.,-1.,0.));
#6680=DIRECTION('',(-0.5,0.,-0.866025403784439));
#6681=DIRECTION('center_axis',(-1.60246890531964E-16,0.,1.));
#6682=DIRECTION('ref_axis',(-1.,0.,-1.60246890531964E-16));
#6683=DIRECTION('',(1.,0.,1.60246890531964E-16));
#6684=DIRECTION('',(0.,-1.,0.));
#6685=DIRECTION('',(-1.,0.,-1.60246890531964E-16));
#6686=DIRECTION('center_axis',(0.866025403784439,0.,0.5));
#6687=DIRECTION('ref_axis',(-0.5,0.,0.866025403784439));
#6688=DIRECTION('',(0.5,0.,-0.866025403784439));
#6689=DIRECTION('',(-0.5,0.,0.866025403784439));
#6690=DIRECTION('center_axis',(0.,1.,0.));
#6691=DIRECTION('ref_axis',(1.,0.,0.));
#6692=DIRECTION('center_axis',(0.,-1.,0.));
#6693=DIRECTION('ref_axis',(0.,0.,-1.));
#6694=DIRECTION('center_axis',(0.,1.,0.));
#6695=DIRECTION('ref_axis',(1.,0.,0.));
#6696=DIRECTION('center_axis',(0.,1.,0.));
#6697=DIRECTION('ref_axis',(1.,0.,0.));
#6698=DIRECTION('center_axis',(0.,1.,0.));
#6699=DIRECTION('ref_axis',(0.,0.,1.));
#6700=DIRECTION('center_axis',(0.,-1.,0.));
#6701=DIRECTION('ref_axis',(1.,0.,0.));
#6702=DIRECTION('center_axis',(0.,-1.,0.));
#6703=DIRECTION('ref_axis',(1.,0.,0.));
#6704=DIRECTION('center_axis',(0.,-1.,0.));
#6705=DIRECTION('ref_axis',(1.,0.,0.));
#6706=DIRECTION('',(0.707106781186547,0.707106781186548,8.65956056235493E-17));
#6707=DIRECTION('center_axis',(0.,-1.,0.));
#6708=DIRECTION('ref_axis',(1.,0.,0.));
#6709=DIRECTION('center_axis',(0.,-1.,0.));
#6710=DIRECTION('ref_axis',(1.,0.,0.));
#6711=DIRECTION('',(0.,1.,0.));
#6712=DIRECTION('center_axis',(0.,1.,0.));
#6713=DIRECTION('ref_axis',(1.,0.,0.));
#6714=DIRECTION('center_axis',(0.,-1.,0.));
#6715=DIRECTION('ref_axis',(1.,0.,0.));
#6716=DIRECTION('',(-0.707106781186547,0.707106781186548,-8.65956056235493E-17));
#6717=DIRECTION('center_axis',(0.,-1.,0.));
#6718=DIRECTION('ref_axis',(0.,0.,-1.));
#6719=DIRECTION('center_axis',(0.,-1.,0.));
#6720=DIRECTION('ref_axis',(1.,0.,0.));
#6721=DIRECTION('center_axis',(0.,1.,0.));
#6722=DIRECTION('ref_axis',(1.,0.,0.));
#6723=DIRECTION('center_axis',(0.,1.,0.));
#6724=DIRECTION('ref_axis',(1.,0.,0.));
#6725=DIRECTION('',(-0.447213595499958,0.894427190999916,-5.47678698264203E-17));
#6726=DIRECTION('center_axis',(0.,-1.,0.));
#6727=DIRECTION('ref_axis',(1.,0.,0.));
#6728=DIRECTION('',(0.,1.,0.));
#8114=CARTESIAN_POINT('',(0.,0.,0.));
#8115=CARTESIAN_POINT('Origin',(0.0866025403784439,-0.4,-0.15));
#8116=CARTESIAN_POINT('',(0.173205080756888,-0.4,0.));
#8117=CARTESIAN_POINT('',(0.0866025403784439,-0.4,-0.15));
#8118=CARTESIAN_POINT('',(0.173205080756888,-0.4,0.));
#8119=CARTESIAN_POINT('',(0.0866025403784439,-0.64,-0.15));
#8120=CARTESIAN_POINT('',(0.0866025403784439,-0.4,-0.15));
#8121=CARTESIAN_POINT('',(0.173205080756888,-0.64,0.));
#8122=CARTESIAN_POINT('',(0.173205080756888,-0.64,0.));
#8123=CARTESIAN_POINT('',(0.173205080756888,-0.4,0.));
#8124=CARTESIAN_POINT('Origin',(-0.0866025403784438,-0.4,-0.15));
#8125=CARTESIAN_POINT('',(-0.0866025403784438,-0.4,-0.15));
#8126=CARTESIAN_POINT('',(0.0866025403784439,-0.4,-0.15));
#8127=CARTESIAN_POINT('',(-0.0866025403784438,-0.64,-0.15));
#8128=CARTESIAN_POINT('',(-0.0866025403784438,-0.4,-0.15));
#8129=CARTESIAN_POINT('',(0.0866025403784439,-0.64,-0.15));
#8130=CARTESIAN_POINT('Origin',(-0.173205080756888,-0.4,-2.77555756156289E-17));
#8131=CARTESIAN_POINT('',(-0.173205080756888,-0.4,-2.12115047744981E-17));
#8132=CARTESIAN_POINT('',(-0.0866025403784438,-0.4,-0.15));
#8133=CARTESIAN_POINT('',(-0.173205080756888,-0.64,-2.77555756156289E-17));
#8134=CARTESIAN_POINT('',(-0.173205080756888,-0.4,-2.12115047744981E-17));
#8135=CARTESIAN_POINT('',(-0.0866025403784438,-0.64,-0.15));
#8136=CARTESIAN_POINT('Origin',(-0.0866025403784439,-0.4,0.15));
#8137=CARTESIAN_POINT('',(-0.0866025403784439,-0.4,0.15));
#8138=CARTESIAN_POINT('',(-0.173205080756888,-0.4,-2.12115047744981E-17));
#8139=CARTESIAN_POINT('',(-0.0866025403784439,-0.64,0.15));
#8140=CARTESIAN_POINT('',(-0.0866025403784439,-0.4,0.15));
#8141=CARTESIAN_POINT('',(-0.173205080756888,-0.64,-2.12115047744981E-17));
#8142=CARTESIAN_POINT('Origin',(0.0866025403784439,-0.4,0.15));
#8143=CARTESIAN_POINT('',(0.0866025403784439,-0.4,0.15));
#8144=CARTESIAN_POINT('',(-0.0866025403784439,-0.4,0.15));
#8145=CARTESIAN_POINT('',(0.0866025403784439,-0.64,0.15));
#8146=CARTESIAN_POINT('',(0.0866025403784439,-0.4,0.15));
#8147=CARTESIAN_POINT('',(-0.0866025403784439,-0.64,0.15));
#8148=CARTESIAN_POINT('Origin',(0.173205080756888,-0.4,0.));
#8149=CARTESIAN_POINT('',(0.0866025403784439,-0.4,0.15));
#8150=CARTESIAN_POINT('',(0.0866025403784439,-0.64,0.15));
#8151=CARTESIAN_POINT('Origin',(0.,-0.4,-2.77555756156289E-17));
#8152=CARTESIAN_POINT('Origin',(0.,-0.64,-2.77555756156289E-17));
#8153=CARTESIAN_POINT('Origin',(0.,-1.,0.));
#8154=CARTESIAN_POINT('',(-0.1954,-1.,2.39295984553393E-17));
#8155=CARTESIAN_POINT('Origin',(0.,-1.,0.));
#8156=CARTESIAN_POINT('Origin',(0.3,0.4,0.));
#8157=CARTESIAN_POINT('',(-0.3,0.4,-3.67394039744206E-17));
#8158=CARTESIAN_POINT('Origin',(0.,0.4,0.));
#8159=CARTESIAN_POINT('Origin',(0.,0.375,0.));
#8160=CARTESIAN_POINT('',(-0.35,0.35,-4.28626379701573E-17));
#8161=CARTESIAN_POINT('Origin',(0.,0.35,0.));
#8162=CARTESIAN_POINT('',(-0.325,0.375,-3.9801020972289E-17));
#8163=CARTESIAN_POINT('Origin',(0.,0.19,0.));
#8164=CARTESIAN_POINT('',(-0.35,0.03,-4.28626379701574E-17));
#8165=CARTESIAN_POINT('Origin',(0.,0.03,0.));
#8166=CARTESIAN_POINT('',(-0.35,0.19,-4.28626379701574E-17));
#8167=CARTESIAN_POINT('Origin',(0.,0.0149999999999999,0.));
#8168=CARTESIAN_POINT('',(-0.32,-3.29597460435593E-17,-3.91886975727153E-17));
#8169=CARTESIAN_POINT('Origin',(0.,0.,0.));
#8170=CARTESIAN_POINT('',(-0.335,0.0149999999999999,-4.10256677714363E-17));
#8171=CARTESIAN_POINT('Origin',(0.22,0.,0.));
#8172=CARTESIAN_POINT('',(-0.22,-6.93889390390723E-18,-2.69422295812418E-17));
#8173=CARTESIAN_POINT('Origin',(0.,0.,0.));
#8174=CARTESIAN_POINT('Origin',(0.,-0.02,0.));
#8175=CARTESIAN_POINT('',(-0.1954,-0.0492,2.39295984553393E-17));
#8176=CARTESIAN_POINT('Origin',(0.,-0.0492,0.));
#8177=CARTESIAN_POINT('',(-0.21,-0.02,-2.57175827820944E-17));
#8178=CARTESIAN_POINT('Origin',(0.,-0.8,0.));
#8179=CARTESIAN_POINT('',(-0.1954,-0.8,-2.39295984553393E-17));
#8240=UNCERTAINTY_MEASURE_WITH_UNIT(LENGTH_MEASURE(0.001),#8267,
'DISTANCE_ACCURACY_VALUE',
'Maximum model space distance between geometric entities at asserted c
onnectivities');
#8241=UNCERTAINTY_MEASURE_WITH_UNIT(LENGTH_MEASURE(0.001),#8267,
'DISTANCE_ACCURACY_VALUE',
'Maximum model space distance between geometric entities at asserted c
onnectivities');
#8265=(
GEOMETRIC_REPRESENTATION_CONTEXT(3)
GLOBAL_UNCERTAINTY_ASSIGNED_CONTEXT((#8240))
GLOBAL_UNIT_ASSIGNED_CONTEXT((#8267,#8269,#8270))
REPRESENTATION_CONTEXT('','3D')
);
#8266=(
GEOMETRIC_REPRESENTATION_CONTEXT(3)
GLOBAL_UNCERTAINTY_ASSIGNED_CONTEXT((#8241))
GLOBAL_UNIT_ASSIGNED_CONTEXT((#8267,#8269,#8270))
REPRESENTATION_CONTEXT('','3D')
);
#8267=(
LENGTH_UNIT()
NAMED_UNIT(*)
SI_UNIT(.CENTI.,.METRE.)
);
#8269=(
NAMED_UNIT(*)
PLANE_ANGLE_UNIT()
SI_UNIT($,.RADIAN.)
);
#8270=(
NAMED_UNIT(*)
SI_UNIT($,.STERADIAN.)
SOLID_ANGLE_UNIT()
);
#8294=SHAPE_DEFINITION_REPRESENTATION(#8320,#8381);
#8320=PRODUCT_DEFINITION_SHAPE('',$,#8406);
#8381=SHAPE_REPRESENTATION('',(#5321),#8265);
#8382=PRODUCT_DEFINITION_CONTEXT('part definition',#8456,'design');
#8406=PRODUCT_DEFINITION('M4x10 Cap Screw','M4x10 Cap Screw',
#8430,#8382);
#8430=PRODUCT_DEFINITION_FORMATION('',$,#8481);
#8456=APPLICATION_CONTEXT(
'Core Data for Automotive Mechanical Design Process');
#8457=PRODUCT_CONTEXT('part definition',#8456,'mechanical');
#8481=PRODUCT('M4x10 Cap Screw','M4x10 Cap Screw',
'M4x10 Cap Screw',(#8457));
#8538=COLOUR_RGB('Black',0.12,0.14,0.17);
#8539=FILL_AREA_STYLE_COLOUR('',#8538);
#8540=FILL_AREA_STYLE('',(#8539));
#8541=SURFACE_STYLE_FILL_AREA(#8540);
#8542=SURFACE_SIDE_STYLE('',(#8541));
#8543=SURFACE_STYLE_USAGE(.BOTH.,#8542);
#8544=PRESENTATION_STYLE_ASSIGNMENT((#8543));
ENDSEC;
END-ISO-10303-21;
